ISO-10303-21;
HEADER;
/* Generated by software containing ST-Developer
 * from STEP Tools, Inc. (www.steptools.com) 
 */

FILE_DESCRIPTION(
/* description */ ('Bin tilter linkage'),
/* implementation_level */ '2;1');

FILE_NAME(
/* name */ 'Screw keeper fastener (7).step',
/* time_stamp */ '2026-10-28T03:26:24-07:00',
/* author */ (''),
/* organization */ (''),
/* preprocessor_version */ 'ST-DEVELOPER v20.2',
/* originating_system */ 'Autodesk Translation Framework v15.17.0.0',
/* authorisation */ '');

FILE_SCHEMA (('AUTOMOTIVE_DESIGN { 1 0 10303 214 3 1 1 }'));
ENDSEC;

DATA;
#10=MECHANICAL_DESIGN_GEOMETRIC_PRESENTATION_REPRESENTATION('',(#888),#23728);
#676=SHAPE_REPRESENTATION_RELATIONSHIP('SRR','None',#24140,#782);
#782=ADVANCED_BREP_SHAPE_REPRESENTATION('',(#1002),#23640);
#888=STYLED_ITEM('',(#24772),#1002);
#1002=MANIFOLD_SOLID_BREP('Body1',#12418);
#1232=FACE_BOUND('',#3034,.T.);
#1599=PLANE('',#14154);
#1600=PLANE('',#14159);
#1601=PLANE('',#14162);
#2111=FACE_OUTER_BOUND('',#3033,.T.);
#2112=FACE_OUTER_BOUND('',#3035,.T.);
#2113=FACE_OUTER_BOUND('',#3036,.T.);
#2114=FACE_OUTER_BOUND('',#3037,.T.);
#2115=FACE_OUTER_BOUND('',#3038,.T.);
#3033=EDGE_LOOP('',(#9285));
#3034=EDGE_LOOP('',(#9286));
#3035=EDGE_LOOP('',(#9287,#9288,#9289,#9290));
#3036=EDGE_LOOP('',(#9291));
#3037=EDGE_LOOP('',(#9292,#9293,#9294,#9295));
#3038=EDGE_LOOP('',(#9296));
#4077=LINE('',#20763,#4752);
#4078=LINE('',#20767,#4753);
#4752=VECTOR('',#16668,0.35);
#4753=VECTOR('',#16673,0.2);
#5427=CIRCLE('',#14155,0.35);
#5428=CIRCLE('',#14156,0.2);
#5429=CIRCLE('',#14158,0.35);
#5430=CIRCLE('',#14161,0.2);
#6261=VERTEX_POINT('',#20756);
#6262=VERTEX_POINT('',#20758);
#6263=VERTEX_POINT('',#20761);
#6264=VERTEX_POINT('',#20766);
#7382=EDGE_CURVE('',#6261,#6261,#5427,.T.);
#7383=EDGE_CURVE('',#6262,#6262,#5428,.T.);
#7384=EDGE_CURVE('',#6263,#6263,#5429,.T.);
#7385=EDGE_CURVE('',#6263,#6261,#4077,.T.);
#7386=EDGE_CURVE('',#6262,#6264,#4078,.T.);
#7387=EDGE_CURVE('',#6264,#6264,#5430,.T.);
#9285=ORIENTED_EDGE('',*,*,#7382,.F.);
#9286=ORIENTED_EDGE('',*,*,#7383,.T.);
#9287=ORIENTED_EDGE('',*,*,#7384,.F.);
#9288=ORIENTED_EDGE('',*,*,#7385,.T.);
#9289=ORIENTED_EDGE('',*,*,#7382,.T.);
#9290=ORIENTED_EDGE('',*,*,#7385,.F.);
#9291=ORIENTED_EDGE('',*,*,#7384,.T.);
#9292=ORIENTED_EDGE('',*,*,#7383,.F.);
#9293=ORIENTED_EDGE('',*,*,#7386,.T.);
#9294=ORIENTED_EDGE('',*,*,#7387,.T.);
#9295=ORIENTED_EDGE('',*,*,#7386,.F.);
#9296=ORIENTED_EDGE('',*,*,#7387,.F.);
#11381=CYLINDRICAL_SURFACE('',#14157,0.35);
#11382=CYLINDRICAL_SURFACE('',#14160,0.2);
#11836=ADVANCED_FACE('',(#2111,#1232),#1599,.F.);
#11837=ADVANCED_FACE('',(#2112),#11381,.T.);
#11838=ADVANCED_FACE('',(#2113),#1600,.T.);
#11839=ADVANCED_FACE('',(#2114),#11382,.T.);
#11840=ADVANCED_FACE('',(#2115),#1601,.F.);
#12418=CLOSED_SHELL('',(#11836,#11837,#11838,#11839,#11840));
#14153=AXIS2_PLACEMENT_3D('',#20754,#16656,#16657);
#14154=AXIS2_PLACEMENT_3D('',#20755,#16658,#16659);
#14155=AXIS2_PLACEMENT_3D('',#20757,#16660,#16661);
#14156=AXIS2_PLACEMENT_3D('',#20759,#16662,#16663);
#14157=AXIS2_PLACEMENT_3D('',#20760,#16664,#16665);
#14158=AXIS2_PLACEMENT_3D('',#20762,#16666,#16667);
#14159=AXIS2_PLACEMENT_3D('',#20764,#16669,#16670);
#14160=AXIS2_PLACEMENT_3D('',#20765,#16671,#16672);
#14161=AXIS2_PLACEMENT_3D('',#20768,#16674,#16675);
#14162=AXIS2_PLACEMENT_3D('',#20769,#16676,#16677);
#16656=DIRECTION('axis',(0.,0.,1.));
#16657=DIRECTION('refdir',(1.,0.,0.));
#16658=DIRECTION('center_axis',(1.,0.,0.));
#16659=DIRECTION('ref_axis',(0.,0.,-1.));
#16660=DIRECTION('center_axis',(1.,0.,0.));
#16661=DIRECTION('ref_axis',(0.,0.,-1.));
#16662=DIRECTION('center_axis',(1.,0.,0.));
#16663=DIRECTION('ref_axis',(0.,0.,-1.));
#16664=DIRECTION('center_axis',(1.,0.,0.));
#16665=DIRECTION('ref_axis',(0.,0.,-1.));
#16666=DIRECTION('center_axis',(1.,0.,0.));
#16667=DIRECTION('ref_axis',(0.,0.,-1.));
#16668=DIRECTION('',(-1.,0.,0.));
#16669=DIRECTION('center_axis',(1.,0.,0.));
#16670=DIRECTION('ref_axis',(0.,0.,-1.));
#16671=DIRECTION('center_axis',(1.,0.,0.));
#16672=DIRECTION('ref_axis',(0.,0.,-1.));
#16673=DIRECTION('',(-1.,0.,0.));
#16674=DIRECTION('center_axis',(1.,0.,0.));
#16675=DIRECTION('ref_axis',(0.,0.,-1.));
#16676=DIRECTION('center_axis',(1.,0.,0.));
#16677=DIRECTION('ref_axis',(0.,0.,-1.));
#20754=CARTESIAN_POINT('',(0.,0.,0.));
#20755=CARTESIAN_POINT('Origin',(1.2,-4.5,6.15));
#20756=CARTESIAN_POINT('',(1.2,-4.5,6.5));
#20757=CARTESIAN_POINT('Origin',(1.2,-4.5,6.15));
#20758=CARTESIAN_POINT('',(1.2,-4.5,6.35));
#20759=CARTESIAN_POINT('Origin',(1.2,-4.5,6.15));
#20760=CARTESIAN_POINT('Origin',(1.2,-4.5,6.15));
#20761=CARTESIAN_POINT('',(1.6,-4.5,6.5));
#20762=CARTESIAN_POINT('Origin',(1.6,-4.5,6.15));
#20763=CARTESIAN_POINT('',(1.2,-4.5,6.5));
#20764=CARTESIAN_POINT('Origin',(1.6,-4.5,6.15));
#20765=CARTESIAN_POINT('Origin',(0.5,-4.5,6.15));
#20766=CARTESIAN_POINT('',(0.5,-4.5,6.35));
#20767=CARTESIAN_POINT('',(0.5,-4.5,6.35));
#20768=CARTESIAN_POINT('Origin',(0.5,-4.5,6.15));
#20769=CARTESIAN_POINT('Origin',(0.5,-4.5,6.15));
#23523=UNCERTAINTY_MEASURE_WITH_UNIT(LENGTH_MEASURE(0.001),#23729,
'DISTANCE_ACCURACY_VALUE',
'Maximum model space distance between geometric entities at asserted c
onnectivities');
#23611=UNCERTAINTY_MEASURE_WITH_UNIT(LENGTH_MEASURE(0.001),#23729,
'DISTANCE_ACCURACY_VALUE',
'Maximum model space distance between geometric entities at asserted c
onnectivities');
#23640=(
GEOMETRIC_REPRESENTATION_CONTEXT(3)
GLOBAL_UNCERTAINTY_ASSIGNED_CONTEXT((#23523))
GLOBAL_UNIT_ASSIGNED_CONTEXT((#23729,#23731,#23732))
REPRESENTATION_CONTEXT('','3D')
);
#23728=(
GEOMETRIC_REPRESENTATION_CONTEXT(3)
GLOBAL_UNCERTAINTY_ASSIGNED_CONTEXT((#23611))
GLOBAL_UNIT_ASSIGNED_CONTEXT((#23729,#23731,#23732))
REPRESENTATION_CONTEXT('','3D')
);
#23729=(
LENGTH_UNIT()
NAMED_UNIT(*)
SI_UNIT(.CENTI.,.METRE.)
);
#23731=(
NAMED_UNIT(*)
PLANE_ANGLE_UNIT()
SI_UNIT($,.RADIAN.)
);
#23732=(
NAMED_UNIT(*)
SI_UNIT($,.STERADIAN.)
SOLID_ANGLE_UNIT()
);
#23761=SHAPE_DEFINITION_REPRESENTATION(#23877,#24140);
#23877=PRODUCT_DEFINITION_SHAPE('',$,#24257);
#24140=SHAPE_REPRESENTATION('',(#14153),#23640);
#24228=PRODUCT_DEFINITION_CONTEXT('part definition',#24578,'design');
#24257=PRODUCT_DEFINITION('Screw keeper fastener (7)',
'Screw keeper fastener (7)',#24373,#24228);
#24373=PRODUCT_DEFINITION_FORMATION('',$,#24608);
#24578=APPLICATION_CONTEXT(
'Core Data for Automotive Mechanical Design Process');
#24579=PRODUCT_CONTEXT('part definition',#24578,'mechanical');
#24608=PRODUCT('Screw keeper fastener (7)','Screw keeper fastener (7)',
'Screw keeper fastener (7)',(#24579));
#24766=COLOUR_RGB('Black',0.12,0.14,0.17);
#24767=FILL_AREA_STYLE_COLOUR('',#24766);
#24768=FILL_AREA_STYLE('',(#24767));
#24769=SURFACE_STYLE_FILL_AREA(#24768);
#24770=SURFACE_SIDE_STYLE('',(#24769));
#24771=SURFACE_STYLE_USAGE(.BOTH.,#24770);
#24772=PRESENTATION_STYLE_ASSIGNMENT((#24771));
ENDSEC;
END-ISO-10303-21;
